ISO-10303-21;
HEADER;
/* Generated by software containing ST-Developer
 * from STEP Tools, Inc. (www.steptools.com) 
 */

FILE_DESCRIPTION(
/* description */ ('Jaw-coupled motor to shaft test stand'),
/* implementation_level */ '2;1');

FILE_NAME(
/* name */ 'Mounting reducer (1).step',
/* time_stamp */ '2026-10-27T10:46:06-07:00',
/* author */ (''),
/* organization */ (''),
/* preprocessor_version */ 'ST-DEVELOPER v20.2',
/* originating_system */ 'Autodesk Translation Framework v15.17.0.0',
/* authorisation */ '');

FILE_SCHEMA (('AUTOMOTIVE_DESIGN { 1 0 10303 214 3 1 1 }'));
ENDSEC;

DATA;
#10=MECHANICAL_DESIGN_GEOMETRIC_PRESENTATION_REPRESENTATION('',(#344),#19361);
#280=SHAPE_REPRESENTATION_RELATIONSHIP('SRR','None',#19494,#312);
#312=ADVANCED_BREP_SHAPE_REPRESENTATION('',(#377),#19330);
#344=STYLED_ITEM('',(#19739),#377);
#377=MANIFOLD_SOLID_BREP('Body1',#10988);
#417=FACE_BOUND('',#1687,.T.);
#418=FACE_BOUND('',#1689,.T.);
#536=PLANE('',#11430);
#537=PLANE('',#11431);
#1050=FACE_OUTER_BOUND('',#1684,.T.);
#1051=FACE_OUTER_BOUND('',#1685,.T.);
#1052=FACE_OUTER_BOUND('',#1686,.T.);
#1053=FACE_OUTER_BOUND('',#1688,.T.);
#1684=EDGE_LOOP('',(#7466,#7467,#7468,#7469));
#1685=EDGE_LOOP('',(#7470,#7471,#7472,#7473));
#1686=EDGE_LOOP('',(#7474));
#1687=EDGE_LOOP('',(#7475));
#1688=EDGE_LOOP('',(#7476));
#1689=EDGE_LOOP('',(#7477));
#2419=LINE('',#15566,#3572);
#2420=LINE('',#15572,#3573);
#3572=VECTOR('',#12490,0.425);
#3573=VECTOR('',#12497,0.645);
#4697=CIRCLE('',#11425,0.425);
#4698=CIRCLE('',#11426,0.425);
#4699=CIRCLE('',#11428,0.645);
#4700=CIRCLE('',#11429,0.645);
#4983=VERTEX_POINT('',#15563);
#4984=VERTEX_POINT('',#15565);
#4985=VERTEX_POINT('',#15569);
#4986=VERTEX_POINT('',#15571);
#5944=EDGE_CURVE('',#4983,#4983,#4697,.T.);
#5945=EDGE_CURVE('',#4983,#4984,#2419,.T.);
#5946=EDGE_CURVE('',#4984,#4984,#4698,.T.);
#5947=EDGE_CURVE('',#4985,#4985,#4699,.T.);
#5948=EDGE_CURVE('',#4985,#4986,#2420,.T.);
#5949=EDGE_CURVE('',#4986,#4986,#4700,.T.);
#7466=ORIENTED_EDGE('',*,*,#5944,.F.);
#7467=ORIENTED_EDGE('',*,*,#5945,.T.);
#7468=ORIENTED_EDGE('',*,*,#5946,.T.);
#7469=ORIENTED_EDGE('',*,*,#5945,.F.);
#7470=ORIENTED_EDGE('',*,*,#5947,.F.);
#7471=ORIENTED_EDGE('',*,*,#5948,.T.);
#7472=ORIENTED_EDGE('',*,*,#5949,.T.);
#7473=ORIENTED_EDGE('',*,*,#5948,.F.);
#7474=ORIENTED_EDGE('',*,*,#5947,.T.);
#7475=ORIENTED_EDGE('',*,*,#5944,.T.);
#7476=ORIENTED_EDGE('',*,*,#5949,.F.);
#7477=ORIENTED_EDGE('',*,*,#5946,.F.);
#10278=CYLINDRICAL_SURFACE('',#11424,0.425);
#10279=CYLINDRICAL_SURFACE('',#11427,0.645);
#10392=ADVANCED_FACE('',(#1050),#10278,.F.);
#10393=ADVANCED_FACE('',(#1051),#10279,.T.);
#10394=ADVANCED_FACE('',(#1052,#417),#536,.T.);
#10395=ADVANCED_FACE('',(#1053,#418),#537,.F.);
#10988=CLOSED_SHELL('',(#10392,#10393,#10394,#10395));
#11423=AXIS2_PLACEMENT_3D('',#15561,#12484,#12485);
#11424=AXIS2_PLACEMENT_3D('',#15562,#12486,#12487);
#11425=AXIS2_PLACEMENT_3D('',#15564,#12488,#12489);
#11426=AXIS2_PLACEMENT_3D('',#15567,#12491,#12492);
#11427=AXIS2_PLACEMENT_3D('',#15568,#12493,#12494);
#11428=AXIS2_PLACEMENT_3D('',#15570,#12495,#12496);
#11429=AXIS2_PLACEMENT_3D('',#15573,#12498,#12499);
#11430=AXIS2_PLACEMENT_3D('',#15574,#12500,#12501);
#11431=AXIS2_PLACEMENT_3D('',#15575,#12502,#12503);
#12484=DIRECTION('axis',(0.,0.,1.));
#12485=DIRECTION('refdir',(1.,0.,0.));
#12486=DIRECTION('center_axis',(0.,0.,1.));
#12487=DIRECTION('ref_axis',(1.,0.,0.));
#12488=DIRECTION('center_axis',(0.,0.,-1.));
#12489=DIRECTION('ref_axis',(1.,0.,0.));
#12490=DIRECTION('',(0.,0.,-1.));
#12491=DIRECTION('center_axis',(0.,0.,-1.));
#12492=DIRECTION('ref_axis',(1.,0.,0.));
#12493=DIRECTION('center_axis',(0.,0.,1.));
#12494=DIRECTION('ref_axis',(1.,0.,0.));
#12495=DIRECTION('center_axis',(0.,0.,1.));
#12496=DIRECTION('ref_axis',(1.,0.,0.));
#12497=DIRECTION('',(0.,0.,-1.));
#12498=DIRECTION('center_axis',(0.,0.,1.));
#12499=DIRECTION('ref_axis',(1.,0.,0.));
#12500=DIRECTION('center_axis',(0.,0.,1.));
#12501=DIRECTION('ref_axis',(1.,0.,0.));
#12502=DIRECTION('center_axis',(0.,0.,1.));
#12503=DIRECTION('ref_axis',(1.,0.,0.));
#15561=CARTESIAN_POINT('',(0.,0.,0.));
#15562=CARTESIAN_POINT('Origin',(4.75,2.,1.2));
#15563=CARTESIAN_POINT('',(4.325,2.,2.4));
#15564=CARTESIAN_POINT('Origin',(4.75,2.,2.4));
#15565=CARTESIAN_POINT('',(4.325,2.,1.2));
#15566=CARTESIAN_POINT('',(4.325,2.,1.2));
#15567=CARTESIAN_POINT('Origin',(4.75,2.,1.2));
#15568=CARTESIAN_POINT('Origin',(4.75,2.,1.2));
#15569=CARTESIAN_POINT('',(4.105,2.,2.4));
#15570=CARTESIAN_POINT('Origin',(4.75,2.,2.4));
#15571=CARTESIAN_POINT('',(4.105,2.,1.2));
#15572=CARTESIAN_POINT('',(4.105,2.,1.2));
#15573=CARTESIAN_POINT('Origin',(4.75,2.,1.2));
#15574=CARTESIAN_POINT('Origin',(4.75,2.,2.4));
#15575=CARTESIAN_POINT('Origin',(4.75,2.,1.2));
#19292=UNCERTAINTY_MEASURE_WITH_UNIT(LENGTH_MEASURE(0.001),#19362,
'DISTANCE_ACCURACY_VALUE',
'Maximum model space distance between geometric entities at asserted c
onnectivities');
#19323=UNCERTAINTY_MEASURE_WITH_UNIT(LENGTH_MEASURE(0.001),#19362,
'DISTANCE_ACCURACY_VALUE',
'Maximum model space distance between geometric entities at asserted c
onnectivities');
#19330=(
GEOMETRIC_REPRESENTATION_CONTEXT(3)
GLOBAL_UNCERTAINTY_ASSIGNED_CONTEXT((#19292))
GLOBAL_UNIT_ASSIGNED_CONTEXT((#19362,#19364,#19365))
REPRESENTATION_CONTEXT('','3D')
);
#19361=(
GEOMETRIC_REPRESENTATION_CONTEXT(3)
GLOBAL_UNCERTAINTY_ASSIGNED_CONTEXT((#19323))
GLOBAL_UNIT_ASSIGNED_CONTEXT((#19362,#19364,#19365))
REPRESENTATION_CONTEXT('','3D')
);
#19362=(
LENGTH_UNIT()
NAMED_UNIT(*)
SI_UNIT(.CENTI.,.METRE.)
);
#19364=(
NAMED_UNIT(*)
PLANE_ANGLE_UNIT()
SI_UNIT($,.RADIAN.)
);
#19365=(
NAMED_UNIT(*)
SI_UNIT($,.STERADIAN.)
SOLID_ANGLE_UNIT()
);
#19372=SHAPE_DEFINITION_REPRESENTATION(#19409,#19494);
#19409=PRODUCT_DEFINITION_SHAPE('',$,#19532);
#19494=SHAPE_REPRESENTATION('',(#11423),#19330);
#19525=PRODUCT_DEFINITION_CONTEXT('part definition',#19638,'design');
#19532=PRODUCT_DEFINITION('Mounting reducer (1)','Mounting reducer (1)',#19569,
#19525);
#19569=PRODUCT_DEFINITION_FORMATION('',$,#19646);
#19638=APPLICATION_CONTEXT(
'Core Data for Automotive Mechanical Design Process');
#19639=PRODUCT_CONTEXT('part definition',#19638,'mechanical');
#19646=PRODUCT('Mounting reducer (1)','Mounting reducer (1)',
'Mounting reducer (1)',(#19639));
#19733=COLOUR_RGB('Sky Blue',0.24,0.69,0.87);
#19734=FILL_AREA_STYLE_COLOUR('',#19733);
#19735=FILL_AREA_STYLE('',(#19734));
#19736=SURFACE_STYLE_FILL_AREA(#19735);
#19737=SURFACE_SIDE_STYLE('',(#19736));
#19738=SURFACE_STYLE_USAGE(.BOTH.,#19737);
#19739=PRESENTATION_STYLE_ASSIGNMENT((#19738));
ENDSEC;
END-ISO-10303-21;
